ISO-10303-21;
HEADER;
/* Generated by software containing ST-Developer
 * from STEP Tools, Inc. (www.steptools.com) 
 */

FILE_DESCRIPTION(
/* description */ ('Four-bar parallelogram arm'),
/* implementation_level */ '2;1');

FILE_NAME(
/* name */ 'Bearing cap (2).step',
/* time_stamp */ '2026-10-28T03:24:55-07:00',
/* author */ (''),
/* organization */ (''),
/* preprocessor_version */ 'ST-DEVELOPER v20.2',
/* originating_system */ 'Autodesk Translation Framework v15.17.0.0',
/* authorisation */ '');

FILE_SCHEMA (('AUTOMOTIVE_DESIGN { 1 0 10303 214 3 1 1 }'));
ENDSEC;

DATA;
#10=MECHANICAL_DESIGN_GEOMETRIC_PRESENTATION_REPRESENTATION('',(#644),#14512);
#544=SHAPE_REPRESENTATION_RELATIONSHIP('SRR','None',#14766,#594);
#594=ADVANCED_BREP_SHAPE_REPRESENTATION('',(#701),#14481);
#644=STYLED_ITEM('',(#15087),#701);
#701=MANIFOLD_SOLID_BREP('Body1',#7349);
#851=FACE_BOUND('',#1924,.T.);
#852=FACE_BOUND('',#1925,.T.);
#853=FACE_BOUND('',#1926,.T.);
#854=FACE_BOUND('',#1927,.T.);
#855=FACE_BOUND('',#1928,.T.);
#856=FACE_BOUND('',#1930,.T.);
#857=FACE_BOUND('',#1931,.T.);
#858=FACE_BOUND('',#1932,.T.);
#859=FACE_BOUND('',#1933,.T.);
#860=FACE_BOUND('',#1934,.T.);
#1101=PLANE('',#8329);
#1102=PLANE('',#8330);
#1381=FACE_OUTER_BOUND('',#1917,.T.);
#1382=FACE_OUTER_BOUND('',#1918,.T.);
#1383=FACE_OUTER_BOUND('',#1919,.T.);
#1384=FACE_OUTER_BOUND('',#1920,.T.);
#1385=FACE_OUTER_BOUND('',#1921,.T.);
#1386=FACE_OUTER_BOUND('',#1922,.T.);
#1387=FACE_OUTER_BOUND('',#1923,.T.);
#1388=FACE_OUTER_BOUND('',#1929,.T.);
#1917=EDGE_LOOP('',(#5730,#5731,#5732,#5733));
#1918=EDGE_LOOP('',(#5734,#5735,#5736,#5737));
#1919=EDGE_LOOP('',(#5738,#5739,#5740,#5741));
#1920=EDGE_LOOP('',(#5742,#5743,#5744,#5745));
#1921=EDGE_LOOP('',(#5746,#5747,#5748,#5749));
#1922=EDGE_LOOP('',(#5750,#5751,#5752,#5753));
#1923=EDGE_LOOP('',(#5754));
#1924=EDGE_LOOP('',(#5755));
#1925=EDGE_LOOP('',(#5756));
#1926=EDGE_LOOP('',(#5757));
#1927=EDGE_LOOP('',(#5758));
#1928=EDGE_LOOP('',(#5759));
#1929=EDGE_LOOP('',(#5760));
#1930=EDGE_LOOP('',(#5761));
#1931=EDGE_LOOP('',(#5762));
#1932=EDGE_LOOP('',(#5763));
#1933=EDGE_LOOP('',(#5764));
#1934=EDGE_LOOP('',(#5765));
#2509=LINE('',#12856,#2903);
#2510=LINE('',#12862,#2904);
#2511=LINE('',#12868,#2905);
#2512=LINE('',#12874,#2906);
#2513=LINE('',#12880,#2907);
#2514=LINE('',#12886,#2908);
#2903=VECTOR('',#9917,0.225000000000001);
#2904=VECTOR('',#9924,0.225000000000001);
#2905=VECTOR('',#9931,0.225000000000001);
#2906=VECTOR('',#9938,0.225000000000001);
#2907=VECTOR('',#9945,1.02);
#2908=VECTOR('',#9952,2.2);
#3268=CIRCLE('',#8312,0.225000000000001);
#3269=CIRCLE('',#8313,0.225000000000001);
#3270=CIRCLE('',#8315,0.225000000000001);
#3271=CIRCLE('',#8316,0.225000000000001);
#3272=CIRCLE('',#8318,0.225000000000001);
#3273=CIRCLE('',#8319,0.225000000000001);
#3274=CIRCLE('',#8321,0.225000000000001);
#3275=CIRCLE('',#8322,0.225000000000001);
#3276=CIRCLE('',#8324,1.02);
#3277=CIRCLE('',#8325,1.02);
#3278=CIRCLE('',#8327,2.2);
#3279=CIRCLE('',#8328,2.2);
#3790=VERTEX_POINT('',#12853);
#3791=VERTEX_POINT('',#12855);
#3792=VERTEX_POINT('',#12859);
#3793=VERTEX_POINT('',#12861);
#3794=VERTEX_POINT('',#12865);
#3795=VERTEX_POINT('',#12867);
#3796=VERTEX_POINT('',#12871);
#3797=VERTEX_POINT('',#12873);
#3798=VERTEX_POINT('',#12877);
#3799=VERTEX_POINT('',#12879);
#3800=VERTEX_POINT('',#12883);
#3801=VERTEX_POINT('',#12885);
#4496=EDGE_CURVE('',#3790,#3790,#3268,.T.);
#4497=EDGE_CURVE('',#3790,#3791,#2509,.T.);
#4498=EDGE_CURVE('',#3791,#3791,#3269,.T.);
#4499=EDGE_CURVE('',#3792,#3792,#3270,.T.);
#4500=EDGE_CURVE('',#3792,#3793,#2510,.T.);
#4501=EDGE_CURVE('',#3793,#3793,#3271,.T.);
#4502=EDGE_CURVE('',#3794,#3794,#3272,.T.);
#4503=EDGE_CURVE('',#3794,#3795,#2511,.T.);
#4504=EDGE_CURVE('',#3795,#3795,#3273,.T.);
#4505=EDGE_CURVE('',#3796,#3796,#3274,.T.);
#4506=EDGE_CURVE('',#3796,#3797,#2512,.T.);
#4507=EDGE_CURVE('',#3797,#3797,#3275,.T.);
#4508=EDGE_CURVE('',#3798,#3798,#3276,.T.);
#4509=EDGE_CURVE('',#3798,#3799,#2513,.T.);
#4510=EDGE_CURVE('',#3799,#3799,#3277,.T.);
#4511=EDGE_CURVE('',#3800,#3800,#3278,.T.);
#4512=EDGE_CURVE('',#3800,#3801,#2514,.T.);
#4513=EDGE_CURVE('',#3801,#3801,#3279,.T.);
#5730=ORIENTED_EDGE('',*,*,#4496,.F.);
#5731=ORIENTED_EDGE('',*,*,#4497,.T.);
#5732=ORIENTED_EDGE('',*,*,#4498,.F.);
#5733=ORIENTED_EDGE('',*,*,#4497,.F.);
#5734=ORIENTED_EDGE('',*,*,#4499,.F.);
#5735=ORIENTED_EDGE('',*,*,#4500,.T.);
#5736=ORIENTED_EDGE('',*,*,#4501,.F.);
#5737=ORIENTED_EDGE('',*,*,#4500,.F.);
#5738=ORIENTED_EDGE('',*,*,#4502,.F.);
#5739=ORIENTED_EDGE('',*,*,#4503,.T.);
#5740=ORIENTED_EDGE('',*,*,#4504,.F.);
#5741=ORIENTED_EDGE('',*,*,#4503,.F.);
#5742=ORIENTED_EDGE('',*,*,#4505,.F.);
#5743=ORIENTED_EDGE('',*,*,#4506,.T.);
#5744=ORIENTED_EDGE('',*,*,#4507,.F.);
#5745=ORIENTED_EDGE('',*,*,#4506,.F.);
#5746=ORIENTED_EDGE('',*,*,#4508,.F.);
#5747=ORIENTED_EDGE('',*,*,#4509,.T.);
#5748=ORIENTED_EDGE('',*,*,#4510,.T.);
#5749=ORIENTED_EDGE('',*,*,#4509,.F.);
#5750=ORIENTED_EDGE('',*,*,#4511,.F.);
#5751=ORIENTED_EDGE('',*,*,#4512,.T.);
#5752=ORIENTED_EDGE('',*,*,#4513,.T.);
#5753=ORIENTED_EDGE('',*,*,#4512,.F.);
#5754=ORIENTED_EDGE('',*,*,#4511,.T.);
#5755=ORIENTED_EDGE('',*,*,#4508,.T.);
#5756=ORIENTED_EDGE('',*,*,#4507,.T.);
#5757=ORIENTED_EDGE('',*,*,#4504,.T.);
#5758=ORIENTED_EDGE('',*,*,#4501,.T.);
#5759=ORIENTED_EDGE('',*,*,#4498,.T.);
#5760=ORIENTED_EDGE('',*,*,#4513,.F.);
#5761=ORIENTED_EDGE('',*,*,#4510,.F.);
#5762=ORIENTED_EDGE('',*,*,#4505,.T.);
#5763=ORIENTED_EDGE('',*,*,#4502,.T.);
#5764=ORIENTED_EDGE('',*,*,#4499,.T.);
#5765=ORIENTED_EDGE('',*,*,#4496,.T.);
#6795=CYLINDRICAL_SURFACE('',#8311,0.225000000000001);
#6796=CYLINDRICAL_SURFACE('',#8314,0.225000000000001);
#6797=CYLINDRICAL_SURFACE('',#8317,0.225000000000001);
#6798=CYLINDRICAL_SURFACE('',#8320,0.225000000000001);
#6799=CYLINDRICAL_SURFACE('',#8323,1.02);
#6800=CYLINDRICAL_SURFACE('',#8326,2.2);
#7086=ADVANCED_FACE('',(#1381),#6795,.F.);
#7087=ADVANCED_FACE('',(#1382),#6796,.F.);
#7088=ADVANCED_FACE('',(#1383),#6797,.F.);
#7089=ADVANCED_FACE('',(#1384),#6798,.F.);
#7090=ADVANCED_FACE('',(#1385),#6799,.F.);
#7091=ADVANCED_FACE('',(#1386),#6800,.T.);
#7092=ADVANCED_FACE('',(#1387,#851,#852,#853,#854,#855),#1101,.T.);
#7093=ADVANCED_FACE('',(#1388,#856,#857,#858,#859,#860),#1102,.F.);
#7349=CLOSED_SHELL('',(#7086,#7087,#7088,#7089,#7090,#7091,#7092,#7093));
#8310=AXIS2_PLACEMENT_3D('',#12851,#9911,#9912);
#8311=AXIS2_PLACEMENT_3D('',#12852,#9913,#9914);
#8312=AXIS2_PLACEMENT_3D('',#12854,#9915,#9916);
#8313=AXIS2_PLACEMENT_3D('',#12857,#9918,#9919);
#8314=AXIS2_PLACEMENT_3D('',#12858,#9920,#9921);
#8315=AXIS2_PLACEMENT_3D('',#12860,#9922,#9923);
#8316=AXIS2_PLACEMENT_3D('',#12863,#9925,#9926);
#8317=AXIS2_PLACEMENT_3D('',#12864,#9927,#9928);
#8318=AXIS2_PLACEMENT_3D('',#12866,#9929,#9930);
#8319=AXIS2_PLACEMENT_3D('',#12869,#9932,#9933);
#8320=AXIS2_PLACEMENT_3D('',#12870,#9934,#9935);
#8321=AXIS2_PLACEMENT_3D('',#12872,#9936,#9937);
#8322=AXIS2_PLACEMENT_3D('',#12875,#9939,#9940);
#8323=AXIS2_PLACEMENT_3D('',#12876,#9941,#9942);
#8324=AXIS2_PLACEMENT_3D('',#12878,#9943,#9944);
#8325=AXIS2_PLACEMENT_3D('',#12881,#9946,#9947);
#8326=AXIS2_PLACEMENT_3D('',#12882,#9948,#9949);
#8327=AXIS2_PLACEMENT_3D('',#12884,#9950,#9951);
#8328=AXIS2_PLACEMENT_3D('',#12887,#9953,#9954);
#8329=AXIS2_PLACEMENT_3D('',#12888,#9955,#9956);
#8330=AXIS2_PLACEMENT_3D('',#12889,#9957,#9958);
#9911=DIRECTION('axis',(0.,0.,1.));
#9912=DIRECTION('refdir',(1.,0.,0.));
#9913=DIRECTION('center_axis',(0.,1.,0.));
#9914=DIRECTION('ref_axis',(1.,0.,0.));
#9915=DIRECTION('center_axis',(0.,1.,0.));
#9916=DIRECTION('ref_axis',(1.,0.,0.));
#9917=DIRECTION('',(0.,1.,0.));
#9918=DIRECTION('center_axis',(0.,-1.,0.));
#9919=DIRECTION('ref_axis',(1.,0.,0.));
#9920=DIRECTION('center_axis',(0.,1.,0.));
#9921=DIRECTION('ref_axis',(1.,0.,0.));
#9922=DIRECTION('center_axis',(0.,1.,0.));
#9923=DIRECTION('ref_axis',(1.,0.,0.));
#9924=DIRECTION('',(0.,1.,0.));
#9925=DIRECTION('center_axis',(0.,-1.,0.));
#9926=DIRECTION('ref_axis',(1.,0.,0.));
#9927=DIRECTION('center_axis',(0.,1.,0.));
#9928=DIRECTION('ref_axis',(1.,0.,0.));
#9929=DIRECTION('center_axis',(0.,1.,0.));
#9930=DIRECTION('ref_axis',(1.,0.,0.));
#9931=DIRECTION('',(0.,1.,0.));
#9932=DIRECTION('center_axis',(0.,-1.,0.));
#9933=DIRECTION('ref_axis',(1.,0.,0.));
#9934=DIRECTION('center_axis',(0.,1.,0.));
#9935=DIRECTION('ref_axis',(1.,0.,0.));
#9936=DIRECTION('center_axis',(0.,1.,0.));
#9937=DIRECTION('ref_axis',(1.,0.,0.));
#9938=DIRECTION('',(0.,1.,0.));
#9939=DIRECTION('center_axis',(0.,-1.,0.));
#9940=DIRECTION('ref_axis',(1.,0.,0.));
#9941=DIRECTION('center_axis',(0.,1.,0.));
#9942=DIRECTION('ref_axis',(1.,0.,0.));
#9943=DIRECTION('center_axis',(0.,-1.,0.));
#9944=DIRECTION('ref_axis',(1.,0.,0.));
#9945=DIRECTION('',(0.,-1.,0.));
#9946=DIRECTION('center_axis',(0.,-1.,0.));
#9947=DIRECTION('ref_axis',(1.,0.,0.));
#9948=DIRECTION('center_axis',(0.,1.,0.));
#9949=DIRECTION('ref_axis',(1.,0.,0.));
#9950=DIRECTION('center_axis',(0.,1.,0.));
#9951=DIRECTION('ref_axis',(1.,0.,0.));
#9952=DIRECTION('',(0.,-1.,0.));
#9953=DIRECTION('center_axis',(0.,1.,0.));
#9954=DIRECTION('ref_axis',(1.,0.,0.));
#9955=DIRECTION('center_axis',(0.,1.,0.));
#9956=DIRECTION('ref_axis',(1.,0.,0.));
#9957=DIRECTION('center_axis',(0.,1.,0.));
#9958=DIRECTION('ref_axis',(1.,0.,0.));
#12851=CARTESIAN_POINT('',(0.,0.,0.));
#12852=CARTESIAN_POINT('Origin',(18.7625631329235,-1.5,6.76256313292354));
#12853=CARTESIAN_POINT('',(18.5375631329235,-1.4,6.76256313292354));
#12854=CARTESIAN_POINT('Origin',(18.7625631329235,-1.4,6.76256313292354));
#12855=CARTESIAN_POINT('',(18.5375631329235,-1.05,6.76256313292354));
#12856=CARTESIAN_POINT('',(18.5375631329235,-1.5,6.76256313292354));
#12857=CARTESIAN_POINT('Origin',(18.7625631329235,-1.05,6.76256313292354));
#12858=CARTESIAN_POINT('Origin',(18.7625631329235,-1.5,9.23743686707646));
#12859=CARTESIAN_POINT('',(18.5375631329235,-1.4,9.23743686707646));
#12860=CARTESIAN_POINT('Origin',(18.7625631329235,-1.4,9.23743686707646));
#12861=CARTESIAN_POINT('',(18.5375631329235,-1.05,9.23743686707646));
#12862=CARTESIAN_POINT('',(18.5375631329235,-1.5,9.23743686707646));
#12863=CARTESIAN_POINT('Origin',(18.7625631329235,-1.05,9.23743686707646));
#12864=CARTESIAN_POINT('Origin',(21.2374368670765,-1.5,9.23743686707646));
#12865=CARTESIAN_POINT('',(21.0124368670765,-1.4,9.23743686707646));
#12866=CARTESIAN_POINT('Origin',(21.2374368670765,-1.4,9.23743686707646));
#12867=CARTESIAN_POINT('',(21.0124368670765,-1.05,9.23743686707646));
#12868=CARTESIAN_POINT('',(21.0124368670765,-1.5,9.23743686707646));
#12869=CARTESIAN_POINT('Origin',(21.2374368670765,-1.05,9.23743686707646));
#12870=CARTESIAN_POINT('Origin',(21.2374368670765,-1.5,6.76256313292354));
#12871=CARTESIAN_POINT('',(21.0124368670765,-1.4,6.76256313292354));
#12872=CARTESIAN_POINT('Origin',(21.2374368670765,-1.4,6.76256313292354));
#12873=CARTESIAN_POINT('',(21.0124368670765,-1.05,6.76256313292354));
#12874=CARTESIAN_POINT('',(21.0124368670765,-1.5,6.76256313292354));
#12875=CARTESIAN_POINT('Origin',(21.2374368670765,-1.05,6.76256313292354));
#12876=CARTESIAN_POINT('Origin',(20.,-1.4,8.));
#12877=CARTESIAN_POINT('',(18.98,-1.05,8.));
#12878=CARTESIAN_POINT('Origin',(20.,-1.05,8.));
#12879=CARTESIAN_POINT('',(18.98,-1.4,8.));
#12880=CARTESIAN_POINT('',(18.98,-1.4,8.));
#12881=CARTESIAN_POINT('Origin',(20.,-1.4,8.));
#12882=CARTESIAN_POINT('Origin',(20.,-1.4,8.));
#12883=CARTESIAN_POINT('',(17.8,-1.05,8.));
#12884=CARTESIAN_POINT('Origin',(20.,-1.05,8.));
#12885=CARTESIAN_POINT('',(17.8,-1.4,8.));
#12886=CARTESIAN_POINT('',(17.8,-1.4,8.));
#12887=CARTESIAN_POINT('Origin',(20.,-1.4,8.));
#12888=CARTESIAN_POINT('Origin',(20.,-1.05,8.));
#12889=CARTESIAN_POINT('Origin',(20.,-1.4,8.));
#14424=UNCERTAINTY_MEASURE_WITH_UNIT(LENGTH_MEASURE(0.001),#14513,
'DISTANCE_ACCURACY_VALUE',
'Maximum model space distance between geometric entities at asserted c
onnectivities');
#14455=UNCERTAINTY_MEASURE_WITH_UNIT(LENGTH_MEASURE(0.001),#14513,
'DISTANCE_ACCURACY_VALUE',
'Maximum model space distance between geometric entities at asserted c
onnectivities');
#14481=(
GEOMETRIC_REPRESENTATION_CONTEXT(3)
GLOBAL_UNCERTAINTY_ASSIGNED_CONTEXT((#14424))
GLOBAL_UNIT_ASSIGNED_CONTEXT((#14513,#14515,#14516))
REPRESENTATION_CONTEXT('','3D')
);
#14512=(
GEOMETRIC_REPRESENTATION_CONTEXT(3)
GLOBAL_UNCERTAINTY_ASSIGNED_CONTEXT((#14455))
GLOBAL_UNIT_ASSIGNED_CONTEXT((#14513,#14515,#14516))
REPRESENTATION_CONTEXT('','3D')
);
#14513=(
LENGTH_UNIT()
NAMED_UNIT(*)
SI_UNIT(.CENTI.,.METRE.)
);
#14515=(
NAMED_UNIT(*)
PLANE_ANGLE_UNIT()
SI_UNIT($,.RADIAN.)
);
#14516=(
NAMED_UNIT(*)
SI_UNIT($,.STERADIAN.)
SOLID_ANGLE_UNIT()
);
#14542=SHAPE_DEFINITION_REPRESENTATION(#14598,#14766);
#14598=PRODUCT_DEFINITION_SHAPE('',$,#14823);
#14766=SHAPE_REPRESENTATION('',(#8310),#14481);
#14797=PRODUCT_DEFINITION_CONTEXT('part definition',#14967,'design');
#14823=PRODUCT_DEFINITION('Bearing cap (2)','Bearing cap (2)',#14879,#14797);
#14879=PRODUCT_DEFINITION_FORMATION('',$,#14994);
#14967=APPLICATION_CONTEXT(
'Core Data for Automotive Mechanical Design Process');
#14968=PRODUCT_CONTEXT('part definition',#14967,'mechanical');
#14994=PRODUCT('Bearing cap (2)','Bearing cap (2)','Bearing cap (2)',(#14968));
#15081=COLOUR_RGB('Grey',0.48,0.52,0.57);
#15082=FILL_AREA_STYLE_COLOUR('',#15081);
#15083=FILL_AREA_STYLE('',(#15082));
#15084=SURFACE_STYLE_FILL_AREA(#15083);
#15085=SURFACE_SIDE_STYLE('',(#15084));
#15086=SURFACE_STYLE_USAGE(.BOTH.,#15085);
#15087=PRESENTATION_STYLE_ASSIGNMENT((#15086));
ENDSEC;
END-ISO-10303-21;
